ISO-10303-21;
HEADER;
/* Generated by software containing ST-Developer
 * from STEP Tools, Inc. (www.steptools.com) 
 */

FILE_DESCRIPTION(
/* description */ (''),
/* implementation_level */ '2;1');

FILE_NAME(
/* name */ 'Plunger_Shaft.step',
/* time_stamp */ '2026-10-23T17:22:31+06:00',
/* author */ (''),
/* organization */ (''),
/* preprocessor_version */ 'ST-DEVELOPER v20.2',
/* originating_system */ 'Autodesk Translation Framework v15.15.0.0',
/* authorisation */ '');

FILE_SCHEMA (('AUTOMOTIVE_DESIGN { 1 0 10303 214 3 1 1 }'));
ENDSEC;

DATA;
#10=MECHANICAL_DESIGN_GEOMETRIC_PRESENTATION_REPRESENTATION('',(#83),#7315);
#63=SHAPE_REPRESENTATION_RELATIONSHIP('SRR','None',#7359,#73);
#73=ADVANCED_BREP_SHAPE_REPRESENTATION('',(#93),#7311);
#83=STYLED_ITEM('',(#7445),#93);
#93=MANIFOLD_SOLID_BREP('Plunger_Shaft',#3220);
#104=CONICAL_SURFACE('',#3685,3.47286361298787,0.785398163397448);
#383=LINE('',#7238,#543);
#384=LINE('',#7246,#544);
#385=LINE('',#7251,#545);
#543=VECTOR('',#4582,3.47286361298787);
#544=VECTOR('',#4593,3.72286361298787);
#545=VECTOR('',#4600,1.51706056234455);
#684=CYLINDRICAL_SURFACE('',#3690,3.72286361298787);
#685=CYLINDRICAL_SURFACE('',#3694,1.51706056234455);
#697=FACE_BOUND('',#1088,.T.);
#721=PLANE('',#3688);
#722=PLANE('',#3692);
#723=PLANE('',#3695);
#896=FACE_OUTER_BOUND('',#1086,.T.);
#897=FACE_OUTER_BOUND('',#1087,.T.);
#898=FACE_OUTER_BOUND('',#1089,.T.);
#899=FACE_OUTER_BOUND('',#1090,.T.);
#900=FACE_OUTER_BOUND('',#1091,.T.);
#901=FACE_OUTER_BOUND('',#1092,.T.);
#1086=EDGE_LOOP('',(#2992,#2993,#2994,#2995));
#1087=EDGE_LOOP('',(#2996));
#1088=EDGE_LOOP('',(#2997));
#1089=EDGE_LOOP('',(#2998,#2999,#3000,#3001));
#1090=EDGE_LOOP('',(#3002));
#1091=EDGE_LOOP('',(#3003,#3004,#3005,#3006));
#1092=EDGE_LOOP('',(#3007));
#1277=CIRCLE('',#3686,3.22286361298787);
#1278=CIRCLE('',#3687,3.72286361298787);
#1279=CIRCLE('',#3689,1.51706056234455);
#1280=CIRCLE('',#3691,3.72286361298787);
#1281=CIRCLE('',#3693,1.51706056234455);
#1593=VERTEX_POINT('',#7235);
#1594=VERTEX_POINT('',#7237);
#1595=VERTEX_POINT('',#7241);
#1596=VERTEX_POINT('',#7244);
#1597=VERTEX_POINT('',#7248);
#2062=EDGE_CURVE('',#1593,#1593,#1277,.T.);
#2063=EDGE_CURVE('',#1593,#1594,#383,.T.);
#2064=EDGE_CURVE('',#1594,#1594,#1278,.T.);
#2065=EDGE_CURVE('',#1595,#1595,#1279,.T.);
#2066=EDGE_CURVE('',#1596,#1596,#1280,.T.);
#2067=EDGE_CURVE('',#1596,#1594,#384,.T.);
#2068=EDGE_CURVE('',#1597,#1597,#1281,.T.);
#2069=EDGE_CURVE('',#1595,#1597,#385,.T.);
#2992=ORIENTED_EDGE('',*,*,#2062,.T.);
#2993=ORIENTED_EDGE('',*,*,#2063,.T.);
#2994=ORIENTED_EDGE('',*,*,#2064,.T.);
#2995=ORIENTED_EDGE('',*,*,#2063,.F.);
#2996=ORIENTED_EDGE('',*,*,#2062,.F.);
#2997=ORIENTED_EDGE('',*,*,#2065,.T.);
#2998=ORIENTED_EDGE('',*,*,#2066,.F.);
#2999=ORIENTED_EDGE('',*,*,#2067,.T.);
#3000=ORIENTED_EDGE('',*,*,#2064,.F.);
#3001=ORIENTED_EDGE('',*,*,#2067,.F.);
#3002=ORIENTED_EDGE('',*,*,#2068,.F.);
#3003=ORIENTED_EDGE('',*,*,#2065,.F.);
#3004=ORIENTED_EDGE('',*,*,#2069,.T.);
#3005=ORIENTED_EDGE('',*,*,#2068,.T.);
#3006=ORIENTED_EDGE('',*,*,#2069,.F.);
#3007=ORIENTED_EDGE('',*,*,#2066,.T.);
#3200=ADVANCED_FACE('',(#896),#104,.T.);
#3201=ADVANCED_FACE('',(#897,#697),#721,.T.);
#3202=ADVANCED_FACE('',(#898),#684,.T.);
#3203=ADVANCED_FACE('',(#899),#722,.F.);
#3204=ADVANCED_FACE('',(#900),#685,.F.);
#3205=ADVANCED_FACE('',(#901),#723,.F.);
#3220=CLOSED_SHELL('',(#3200,#3201,#3202,#3203,#3204,#3205));
#3684=AXIS2_PLACEMENT_3D('',#7233,#4576,#4577);
#3685=AXIS2_PLACEMENT_3D('',#7234,#4578,#4579);
#3686=AXIS2_PLACEMENT_3D('',#7236,#4580,#4581);
#3687=AXIS2_PLACEMENT_3D('',#7239,#4583,#4584);
#3688=AXIS2_PLACEMENT_3D('',#7240,#4585,#4586);
#3689=AXIS2_PLACEMENT_3D('',#7242,#4587,#4588);
#3690=AXIS2_PLACEMENT_3D('',#7243,#4589,#4590);
#3691=AXIS2_PLACEMENT_3D('',#7245,#4591,#4592);
#3692=AXIS2_PLACEMENT_3D('',#7247,#4594,#4595);
#3693=AXIS2_PLACEMENT_3D('',#7249,#4596,#4597);
#3694=AXIS2_PLACEMENT_3D('',#7250,#4598,#4599);
#3695=AXIS2_PLACEMENT_3D('',#7252,#4601,#4602);
#4576=DIRECTION('axis',(0.,0.,1.));
#4577=DIRECTION('refdir',(1.,0.,0.));
#4578=DIRECTION('center_axis',(1.,0.,0.));
#4579=DIRECTION('ref_axis',(0.,-1.,0.));
#4580=DIRECTION('center_axis',(1.,0.,0.));
#4581=DIRECTION('ref_axis',(0.,-1.,0.));
#4582=DIRECTION('',(0.707106781186548,0.707106781186547,-8.65956056235493E-17));
#4583=DIRECTION('center_axis',(-1.,0.,0.));
#4584=DIRECTION('ref_axis',(0.,-1.,0.));
#4585=DIRECTION('center_axis',(-1.,0.,0.));
#4586=DIRECTION('ref_axis',(0.,-1.,0.));
#4587=DIRECTION('center_axis',(1.,0.,0.));
#4588=DIRECTION('ref_axis',(0.,0.,-1.));
#4589=DIRECTION('center_axis',(1.,0.,0.));
#4590=DIRECTION('ref_axis',(0.,-1.,0.));
#4591=DIRECTION('center_axis',(1.,0.,0.));
#4592=DIRECTION('ref_axis',(0.,-1.,0.));
#4593=DIRECTION('',(-1.,0.,0.));
#4594=DIRECTION('center_axis',(1.,0.,0.));
#4595=DIRECTION('ref_axis',(0.,0.,-1.));
#4596=DIRECTION('center_axis',(1.,0.,0.));
#4597=DIRECTION('ref_axis',(0.,0.,-1.));
#4598=DIRECTION('center_axis',(1.,0.,0.));
#4599=DIRECTION('ref_axis',(0.,0.,-1.));
#4600=DIRECTION('',(1.,0.,0.));
#4601=DIRECTION('center_axis',(-1.,0.,0.));
#4602=DIRECTION('ref_axis',(0.,-1.,0.));
#7233=CARTESIAN_POINT('',(0.,0.,0.));
#7234=CARTESIAN_POINT('Origin',(-7.75,0.,0.));
#7235=CARTESIAN_POINT('',(-8.,3.22286361298787,3.94686960773406E-16));
#7236=CARTESIAN_POINT('Origin',(-8.,0.,0.));
#7237=CARTESIAN_POINT('',(-7.5,3.72286361298787,-4.55919300730774E-16));
#7238=CARTESIAN_POINT('',(-7.75,3.47286361298787,-4.2530313075209E-16));
#7239=CARTESIAN_POINT('Origin',(-7.5,0.,0.));
#7240=CARTESIAN_POINT('Origin',(-8.,0.,0.));
#7241=CARTESIAN_POINT('',(-8.,-1.85786336178794E-16,1.51706056234455));
#7242=CARTESIAN_POINT('Origin',(-8.,0.,0.));
#7243=CARTESIAN_POINT('Origin',(0.,0.,0.));
#7244=CARTESIAN_POINT('',(21.22,3.72286361298787,-4.55919300730774E-16));
#7245=CARTESIAN_POINT('Origin',(21.22,0.,0.));
#7246=CARTESIAN_POINT('',(0.,3.72286361298787,4.55919300730774E-16));
#7247=CARTESIAN_POINT('Origin',(-6.41326808244201,0.,0.));
#7248=CARTESIAN_POINT('',(-6.41326808244201,-1.85786336178794E-16,1.51706056234455));
#7249=CARTESIAN_POINT('Origin',(-6.41326808244201,0.,0.));
#7250=CARTESIAN_POINT('Origin',(-8.11443509544501,0.,0.));
#7251=CARTESIAN_POINT('',(-8.11443509544501,-1.85786336178794E-16,1.51706056234455));
#7252=CARTESIAN_POINT('Origin',(21.22,0.,0.));
#7299=UNCERTAINTY_MEASURE_WITH_UNIT(LENGTH_MEASURE(0.01),#7316,
'DISTANCE_ACCURACY_VALUE',
'Maximum model space distance between geometric entities at asserted c
onnectivities');
#7303=UNCERTAINTY_MEASURE_WITH_UNIT(LENGTH_MEASURE(0.01),#7316,
'DISTANCE_ACCURACY_VALUE',
'Maximum model space distance between geometric entities at asserted c
onnectivities');
#7311=(
GEOMETRIC_REPRESENTATION_CONTEXT(3)
GLOBAL_UNCERTAINTY_ASSIGNED_CONTEXT((#7299))
GLOBAL_UNIT_ASSIGNED_CONTEXT((#7316,#7318,#7319))
REPRESENTATION_CONTEXT('','3D')
);
#7315=(
GEOMETRIC_REPRESENTATION_CONTEXT(3)
GLOBAL_UNCERTAINTY_ASSIGNED_CONTEXT((#7303))
GLOBAL_UNIT_ASSIGNED_CONTEXT((#7316,#7318,#7319))
REPRESENTATION_CONTEXT('','3D')
);
#7316=(
LENGTH_UNIT()
NAMED_UNIT(*)
SI_UNIT(.MILLI.,.METRE.)
);
#7318=(
NAMED_UNIT(*)
PLANE_ANGLE_UNIT()
SI_UNIT($,.RADIAN.)
);
#7319=(
NAMED_UNIT(*)
SI_UNIT($,.STERADIAN.)
SOLID_ANGLE_UNIT()
);
#7327=SHAPE_DEFINITION_REPRESENTATION(#7338,#7359);
#7338=PRODUCT_DEFINITION_SHAPE('',$,#7371);
#7359=SHAPE_REPRESENTATION('',(#3684),#7311);
#7363=PRODUCT_DEFINITION_CONTEXT('part definition',#7398,'design');
#7371=PRODUCT_DEFINITION('Plunger_Shaft','Plunger_Shaft',#7382,#7363);
#7382=PRODUCT_DEFINITION_FORMATION('',$,#7407);
#7398=APPLICATION_CONTEXT(
'Core Data for Automotive Mechanical Design Process');
#7399=PRODUCT_CONTEXT('part definition',#7398,'mechanical');
#7407=PRODUCT('Plunger_Shaft','Plunger_Shaft',$,(#7399));
#7439=COLOUR_RGB('Grey',0.48,0.52,0.57);
#7440=FILL_AREA_STYLE_COLOUR('',#7439);
#7441=FILL_AREA_STYLE('',(#7440));
#7442=SURFACE_STYLE_FILL_AREA(#7441);
#7443=SURFACE_SIDE_STYLE('',(#7442));
#7444=SURFACE_STYLE_USAGE(.BOTH.,#7443);
#7445=PRESENTATION_STYLE_ASSIGNMENT((#7444));
ENDSEC;
END-ISO-10303-21;
